ISO-10303-21;
HEADER;
/* Generated by software containing ST-Developer
 * from STEP Tools, Inc. (www.steptools.com) 
 */

FILE_DESCRIPTION(
/* description */ ('STEP AP214'),
/* implementation_level */ '2;1');

FILE_NAME(
/* name */ 'Lock Nut.step',
/* time_stamp */ '2026-11-15T14:55:55-08:00',
/* author */ (''),
/* organization */ (''),
/* preprocessor_version */ 'ST-DEVELOPER v20.2',
/* originating_system */ 'Autodesk Translation Framework v15.17.0.0',
/* authorisation */ '');

FILE_SCHEMA (('AUTOMOTIVE_DESIGN { 1 0 10303 214 3 1 1 }'));
ENDSEC;

DATA;
#10=MECHANICAL_DESIGN_GEOMETRIC_PRESENTATION_REPRESENTATION('',(#930,#931),#57079);
#662=B_SPLINE_CURVE_WITH_KNOTS('',3,(#35659,#35660,#35661,#35662,#35663,
#35664,#35665,#35666,#35667,#35668,#35669,#35670,#35671,#35672,#35673,#35674,
#35675,#35676,#35677,#35678,#35679,#35680,#35681,#35682,#35683,#35684,#35685,
#35686,#35687,#35688,#35689,#35690,#35691,#35692),.UNSPECIFIED.,.T.,.F.,
(4,2,2,2,2,2,2,2,2,2,2,2,2,2,2,2,4),(-0.983408728494514,-0.921936907009434,
-0.860465085524354,-0.799010815947619,-0.737556546370885,-0.676102276794151,
-0.614648007217417,-0.553176185732337,-0.491704364247257,-0.430232542762177,
-0.368760721277097,-0.307306451700363,-0.245852182123629,-0.184397912546894,
-0.12294364297016,-0.06147182148508,0.),.UNSPECIFIED.);
#663=B_SPLINE_CURVE_WITH_KNOTS('',3,(#35695,#35696,#35697,#35698,#35699,
#35700,#35701,#35702,#35703,#35704,#35705,#35706,#35707,#35708,#35709,#35710,
#35711,#35712,#35713,#35714,#35715,#35716,#35717,#35718,#35719,#35720,#35721,
#35722,#35723,#35724,#35725,#35726,#35727,#35728),.UNSPECIFIED.,.T.,.F.,
(4,2,2,2,2,2,2,2,2,2,2,2,2,2,2,2,4),(-0.978506763751944,-0.917349594723415,
-0.856192425694886,-0.795036249254422,-0.733880072813958,-0.672723896373494,
-0.611567719933029,-0.550410550904501,-0.489253381875972,-0.428096212847443,
-0.366939043818914,-0.30578286737845,-0.244626690937986,-0.183470514497522,
-0.122314338057057,-0.0611571690285287,0.),.UNSPECIFIED.);
#872=SHAPE_REPRESENTATION_RELATIONSHIP('SRR','None',#57257,#901);
#901=ADVANCED_BREP_SHAPE_REPRESENTATION('',(#967,#968),#57049);
#930=STYLED_ITEM('',(#57444),#967);
#931=STYLED_ITEM('',(#57444),#968);
#967=MANIFOLD_SOLID_BREP('Body1',#24530);
#968=MANIFOLD_SOLID_BREP('Body2',#24531);
#1069=FACE_BOUND('',#3789,.T.);
#1070=FACE_BOUND('',#3795,.T.);
#1071=FACE_BOUND('',#3797,.T.);
#1072=FACE_BOUND('',#3799,.T.);
#1073=FACE_BOUND('',#3801,.T.);
#1074=FACE_BOUND('',#3811,.T.);
#1454=PLANE('',#25239);
#1455=PLANE('',#25240);
#1456=PLANE('',#25241);
#1457=PLANE('',#25242);
#1458=PLANE('',#25243);
#1459=PLANE('',#25244);
#1460=PLANE('',#25245);
#1461=PLANE('',#25254);
#1462=PLANE('',#25255);
#1463=PLANE('',#25256);
#1464=PLANE('',#25257);
#1465=PLANE('',#25258);
#1466=PLANE('',#25259);
#1467=PLANE('',#25260);
#1468=PLANE('',#25261);
#1469=PLANE('',#25262);
#2118=CONICAL_SURFACE('',#25216,5.4585,0.785398163397448);
#2119=CONICAL_SURFACE('',#25220,6.,0.785398163397449);
#2120=CONICAL_SURFACE('',#25246,2.,0.785398163397445);
#2121=CONICAL_SURFACE('',#25249,1.25,0.78539816339745);
#2341=FACE_OUTER_BOUND('',#3785,.T.);
#2342=FACE_OUTER_BOUND('',#3786,.T.);
#2343=FACE_OUTER_BOUND('',#3787,.T.);
#2344=FACE_OUTER_BOUND('',#3788,.T.);
#2345=FACE_OUTER_BOUND('',#3790,.T.);
#2346=FACE_OUTER_BOUND('',#3791,.T.);
#2347=FACE_OUTER_BOUND('',#3792,.T.);
#2348=FACE_OUTER_BOUND('',#3793,.T.);
#2349=FACE_OUTER_BOUND('',#3794,.T.);
#2350=FACE_OUTER_BOUND('',#3796,.T.);
#2351=FACE_OUTER_BOUND('',#3798,.T.);
#2352=FACE_OUTER_BOUND('',#3800,.T.);
#2353=FACE_OUTER_BOUND('',#3802,.T.);
#2354=FACE_OUTER_BOUND('',#3803,.T.);
#2355=FACE_OUTER_BOUND('',#3804,.T.);
#2356=FACE_OUTER_BOUND('',#3805,.T.);
#2357=FACE_OUTER_BOUND('',#3806,.T.);
#2358=FACE_OUTER_BOUND('',#3807,.T.);
#2359=FACE_OUTER_BOUND('',#3808,.T.);
#2360=FACE_OUTER_BOUND('',#3809,.T.);
#2361=FACE_OUTER_BOUND('',#3810,.T.);
#2362=FACE_OUTER_BOUND('',#3812,.T.);
#2363=FACE_OUTER_BOUND('',#3813,.T.);
#2364=FACE_OUTER_BOUND('',#3814,.T.);
#2365=FACE_OUTER_BOUND('',#3815,.T.);
#2366=FACE_OUTER_BOUND('',#3816,.T.);
#2367=FACE_OUTER_BOUND('',#3817,.T.);
#2368=FACE_OUTER_BOUND('',#3818,.T.);
#3785=EDGE_LOOP('',(#16730,#16731,#16732,#16733));
#3786=EDGE_LOOP('',(#16734,#16735,#16736,#16737,#16738));
#3787=EDGE_LOOP('',(#16739,#16740,#16741,#16742));
#3788=EDGE_LOOP('',(#16743,#16744,#16745,#16746,#16747));
#3789=EDGE_LOOP('',(#16748));
#3790=EDGE_LOOP('',(#16749,#16750,#16751,#16752));
#3791=EDGE_LOOP('',(#16753,#16754,#16755,#16756));
#3792=EDGE_LOOP('',(#16757,#16758,#16759,#16760));
#3793=EDGE_LOOP('',(#16761,#16762,#16763,#16764));
#3794=EDGE_LOOP('',(#16765,#16766,#16767,#16768));
#3795=EDGE_LOOP('',(#16769));
#3796=EDGE_LOOP('',(#16770));
#3797=EDGE_LOOP('',(#16771));
#3798=EDGE_LOOP('',(#16772,#16773,#16774,#16775,#16776,#16777,#16778,#16779));
#3799=EDGE_LOOP('',(#16780));
#3800=EDGE_LOOP('',(#16781,#16782,#16783,#16784,#16785,#16786,#16787,#16788));
#3801=EDGE_LOOP('',(#16789));
#3802=EDGE_LOOP('',(#16790,#16791,#16792,#16793));
#3803=EDGE_LOOP('',(#16794,#16795,#16796,#16797));
#3804=EDGE_LOOP('',(#16798,#16799,#16800,#16801));
#3805=EDGE_LOOP('',(#16802,#16803,#16804,#16805));
#3806=EDGE_LOOP('',(#16806,#16807,#16808,#16809));
#3807=EDGE_LOOP('',(#16810,#16811,#16812,#16813,#16814));
#3808=EDGE_LOOP('',(#16815,#16816,#16817,#16818,#16819));
#3809=EDGE_LOOP('',(#16820));
#3810=EDGE_LOOP('',(#16821));
#3811=EDGE_LOOP('',(#16822,#16823,#16824,#16825,#16826,#16827));
#3812=EDGE_LOOP('',(#16828,#16829,#16830,#16831));
#3813=EDGE_LOOP('',(#16832,#16833,#16834,#16835));
#3814=EDGE_LOOP('',(#16836,#16837,#16838,#16839));
#3815=EDGE_LOOP('',(#16840,#16841,#16842,#16843));
#3816=EDGE_LOOP('',(#16844,#16845,#16846,#16847));
#3817=EDGE_LOOP('',(#16848,#16849,#16850,#16851));
#3818=EDGE_LOOP('',(#16852,#16853,#16854,#16855,#16856,#16857));
#5506=LINE('',#35694,#7473);
#5507=LINE('',#35734,#7474);
#5508=LINE('',#35741,#7475);
#5509=LINE('',#35744,#7476);
#5510=LINE('',#35750,#7477);
#5511=LINE('',#35753,#7478);
#5512=LINE('',#35758,#7479);
#5513=LINE('',#35765,#7480);
#5514=LINE('',#35768,#7481);
#5515=LINE('',#35774,#7482);
#5516=LINE('',#35777,#7483);
#5517=LINE('',#35783,#7484);
#5518=LINE('',#35786,#7485);
#5519=LINE('',#35789,#7486);
#5520=LINE('',#35790,#7487);
#5521=LINE('',#35791,#7488);
#5522=LINE('',#35792,#7489);
#5523=LINE('',#35794,#7490);
#5524=LINE('',#35795,#7491);
#5525=LINE('',#35796,#7492);
#5526=LINE('',#35797,#7493);
#5527=LINE('',#35806,#7494);
#5528=LINE('',#35813,#7495);
#5529=LINE('',#35817,#7496);
#5530=LINE('',#35822,#7497);
#5531=LINE('',#35824,#7498);
#5532=LINE('',#35826,#7499);
#5533=LINE('',#35828,#7500);
#5534=LINE('',#35830,#7501);
#5535=LINE('',#35831,#7502);
#5536=LINE('',#35834,#7503);
#5537=LINE('',#35836,#7504);
#5538=LINE('',#35837,#7505);
#5539=LINE('',#35840,#7506);
#5540=LINE('',#35841,#7507);
#5541=LINE('',#35844,#7508);
#5542=LINE('',#35845,#7509);
#5543=LINE('',#35848,#7510);
#5544=LINE('',#35849,#7511);
#5545=LINE('',#35852,#7512);
#5546=LINE('',#35853,#7513);
#5547=LINE('',#35855,#7514);
#7473=VECTOR('',#28398,1.621);
#7474=VECTOR('',#28403,5.4585);
#7475=VECTOR('',#28412,6.);
#7476=VECTOR('',#28417,5.4585);
#7477=VECTOR('',#28422,1000.);
#7478=VECTOR('',#28425,1000.);
#7479=VECTOR('',#28430,8.5);
#7480=VECTOR('',#28437,1000.);
#7481=VECTOR('',#28440,1000.);
#7482=VECTOR('',#28445,1000.);
#7483=VECTOR('',#28448,1000.);
#7484=VECTOR('',#28453,1000.);
#7485=VECTOR('',#28456,1000.);
#7486=VECTOR('',#28461,1000.);
#7487=VECTOR('',#28462,1000.);
#7488=VECTOR('',#28463,1000.);
#7489=VECTOR('',#28464,1000.);
#7490=VECTOR('',#28467,1000.);
#7491=VECTOR('',#28468,1000.);
#7492=VECTOR('',#28469,1000.);
#7493=VECTOR('',#28470,1000.);
#7494=VECTOR('',#28483,2.);
#7495=VECTOR('',#28490,1.25);
#7496=VECTOR('',#28497,2.);
#7497=VECTOR('',#28502,1000.);
#7498=VECTOR('',#28503,1000.);
#7499=VECTOR('',#28504,1000.);
#7500=VECTOR('',#28505,1000.);
#7501=VECTOR('',#28506,1000.);
#7502=VECTOR('',#28507,1000.);
#7503=VECTOR('',#28510,1000.);
#7504=VECTOR('',#28511,1000.);
#7505=VECTOR('',#28512,1000.);
#7506=VECTOR('',#28515,1000.);
#7507=VECTOR('',#28516,1000.);
#7508=VECTOR('',#28519,1000.);
#7509=VECTOR('',#28520,1000.);
#7510=VECTOR('',#28523,1000.);
#7511=VECTOR('',#28524,1000.);
#7512=VECTOR('',#28527,1000.);
#7513=VECTOR('',#28528,1000.);
#7514=VECTOR('',#28531,1000.);
#9324=CIRCLE('',#25217,5.4585);
#9325=CIRCLE('',#25218,6.);
#9326=CIRCLE('',#25219,5.4585);
#9327=CIRCLE('',#25221,5.4585);
#9328=CIRCLE('',#25222,6.);
#9329=CIRCLE('',#25225,11.);
#9330=CIRCLE('',#25226,11.);
#9331=CIRCLE('',#25228,8.5);
#9332=CIRCLE('',#25229,8.5);
#9333=CIRCLE('',#25231,11.);
#9334=CIRCLE('',#25232,11.);
#9335=CIRCLE('',#25234,11.);
#9336=CIRCLE('',#25235,11.);
#9337=CIRCLE('',#25237,11.);
#9338=CIRCLE('',#25238,11.);
#9339=CIRCLE('',#25247,2.);
#9340=CIRCLE('',#25248,1.8);
#9341=CIRCLE('',#25250,2.);
#9342=CIRCLE('',#25251,1.25);
#9343=CIRCLE('',#25252,2.);
#10543=VERTEX_POINT('',#35658);
#10544=VERTEX_POINT('',#35693);
#10545=VERTEX_POINT('',#35730);
#10546=VERTEX_POINT('',#35731);
#10547=VERTEX_POINT('',#35733);
#10548=VERTEX_POINT('',#35738);
#10549=VERTEX_POINT('',#35740);
#10550=VERTEX_POINT('',#35746);
#10551=VERTEX_POINT('',#35747);
#10552=VERTEX_POINT('',#35749);
#10553=VERTEX_POINT('',#35751);
#10554=VERTEX_POINT('',#35755);
#10555=VERTEX_POINT('',#35757);
#10556=VERTEX_POINT('',#35761);
#10557=VERTEX_POINT('',#35762);
#10558=VERTEX_POINT('',#35764);
#10559=VERTEX_POINT('',#35766);
#10560=VERTEX_POINT('',#35770);
#10561=VERTEX_POINT('',#35771);
#10562=VERTEX_POINT('',#35773);
#10563=VERTEX_POINT('',#35775);
#10564=VERTEX_POINT('',#35779);
#10565=VERTEX_POINT('',#35780);
#10566=VERTEX_POINT('',#35782);
#10567=VERTEX_POINT('',#35784);
#10568=VERTEX_POINT('',#35803);
#10569=VERTEX_POINT('',#35805);
#10570=VERTEX_POINT('',#35809);
#10571=VERTEX_POINT('',#35810);
#10572=VERTEX_POINT('',#35812);
#10573=VERTEX_POINT('',#35820);
#10574=VERTEX_POINT('',#35821);
#10575=VERTEX_POINT('',#35823);
#10576=VERTEX_POINT('',#35825);
#10577=VERTEX_POINT('',#35827);
#10578=VERTEX_POINT('',#35829);
#10579=VERTEX_POINT('',#35833);
#10580=VERTEX_POINT('',#35835);
#10581=VERTEX_POINT('',#35839);
#10582=VERTEX_POINT('',#35843);
#10583=VERTEX_POINT('',#35847);
#10584=VERTEX_POINT('',#35851);
#12910=EDGE_CURVE('',#10543,#10543,#662,.T.);
#12911=EDGE_CURVE('',#10543,#10544,#5506,.T.);
#12912=EDGE_CURVE('',#10544,#10544,#663,.T.);
#12913=EDGE_CURVE('',#10545,#10546,#9324,.T.);
#12914=EDGE_CURVE('',#10546,#10547,#5507,.T.);
#12915=EDGE_CURVE('',#10547,#10547,#9325,.T.);
#12916=EDGE_CURVE('',#10546,#10545,#9326,.T.);
#12917=EDGE_CURVE('',#10548,#10548,#9327,.T.);
#12918=EDGE_CURVE('',#10548,#10549,#5508,.T.);
#12919=EDGE_CURVE('',#10549,#10549,#9328,.T.);
#12920=EDGE_CURVE('',#10545,#10548,#5509,.T.);
#12921=EDGE_CURVE('',#10550,#10551,#9329,.T.);
#12922=EDGE_CURVE('',#10551,#10552,#5510,.T.);
#12923=EDGE_CURVE('',#10553,#10552,#9330,.T.);
#12924=EDGE_CURVE('',#10553,#10550,#5511,.T.);
#12925=EDGE_CURVE('',#10554,#10554,#9331,.T.);
#12926=EDGE_CURVE('',#10554,#10555,#5512,.T.);
#12927=EDGE_CURVE('',#10555,#10555,#9332,.T.);
#12928=EDGE_CURVE('',#10556,#10557,#9333,.T.);
#12929=EDGE_CURVE('',#10557,#10558,#5513,.T.);
#12930=EDGE_CURVE('',#10559,#10558,#9334,.T.);
#12931=EDGE_CURVE('',#10559,#10556,#5514,.T.);
#12932=EDGE_CURVE('',#10560,#10561,#9335,.T.);
#12933=EDGE_CURVE('',#10561,#10562,#5515,.T.);
#12934=EDGE_CURVE('',#10563,#10562,#9336,.T.);
#12935=EDGE_CURVE('',#10563,#10560,#5516,.T.);
#12936=EDGE_CURVE('',#10564,#10565,#9337,.T.);
#12937=EDGE_CURVE('',#10565,#10566,#5517,.T.);
#12938=EDGE_CURVE('',#10567,#10566,#9338,.T.);
#12939=EDGE_CURVE('',#10567,#10564,#5518,.T.);
#12940=EDGE_CURVE('',#10558,#10553,#5519,.T.);
#12941=EDGE_CURVE('',#10552,#10567,#5520,.T.);
#12942=EDGE_CURVE('',#10566,#10563,#5521,.T.);
#12943=EDGE_CURVE('',#10562,#10559,#5522,.T.);
#12944=EDGE_CURVE('',#10550,#10557,#5523,.T.);
#12945=EDGE_CURVE('',#10556,#10561,#5524,.T.);
#12946=EDGE_CURVE('',#10560,#10565,#5525,.T.);
#12947=EDGE_CURVE('',#10564,#10551,#5526,.T.);
#12948=EDGE_CURVE('',#10568,#10568,#9339,.T.);
#12949=EDGE_CURVE('',#10568,#10569,#5527,.T.);
#12950=EDGE_CURVE('',#10569,#10569,#9340,.T.);
#12951=EDGE_CURVE('',#10570,#10571,#9341,.T.);
#12952=EDGE_CURVE('',#10571,#10572,#5528,.T.);
#12953=EDGE_CURVE('',#10572,#10572,#9342,.T.);
#12954=EDGE_CURVE('',#10571,#10570,#9343,.T.);
#12955=EDGE_CURVE('',#10570,#10568,#5529,.T.);
#12956=EDGE_CURVE('',#10573,#10574,#5530,.T.);
#12957=EDGE_CURVE('',#10575,#10573,#5531,.T.);
#12958=EDGE_CURVE('',#10576,#10575,#5532,.T.);
#12959=EDGE_CURVE('',#10577,#10576,#5533,.T.);
#12960=EDGE_CURVE('',#10578,#10577,#5534,.T.);
#12961=EDGE_CURVE('',#10574,#10578,#5535,.T.);
#12962=EDGE_CURVE('',#10579,#10574,#5536,.T.);
#12963=EDGE_CURVE('',#10580,#10579,#5537,.T.);
#12964=EDGE_CURVE('',#10580,#10573,#5538,.T.);
#12965=EDGE_CURVE('',#10581,#10580,#5539,.T.);
#12966=EDGE_CURVE('',#10581,#10575,#5540,.T.);
#12967=EDGE_CURVE('',#10582,#10581,#5541,.T.);
#12968=EDGE_CURVE('',#10582,#10576,#5542,.T.);
#12969=EDGE_CURVE('',#10583,#10582,#5543,.T.);
#12970=EDGE_CURVE('',#10583,#10577,#5544,.T.);
#12971=EDGE_CURVE('',#10584,#10583,#5545,.T.);
#12972=EDGE_CURVE('',#10584,#10578,#5546,.T.);
#12973=EDGE_CURVE('',#10579,#10584,#5547,.T.);
#16730=ORIENTED_EDGE('',*,*,#12910,.F.);
#16731=ORIENTED_EDGE('',*,*,#12911,.T.);
#16732=ORIENTED_EDGE('',*,*,#12912,.F.);
#16733=ORIENTED_EDGE('',*,*,#12911,.F.);
#16734=ORIENTED_EDGE('',*,*,#12913,.T.);
#16735=ORIENTED_EDGE('',*,*,#12914,.T.);
#16736=ORIENTED_EDGE('',*,*,#12915,.F.);
#16737=ORIENTED_EDGE('',*,*,#12914,.F.);
#16738=ORIENTED_EDGE('',*,*,#12916,.T.);
#16739=ORIENTED_EDGE('',*,*,#12917,.F.);
#16740=ORIENTED_EDGE('',*,*,#12918,.T.);
#16741=ORIENTED_EDGE('',*,*,#12919,.T.);
#16742=ORIENTED_EDGE('',*,*,#12918,.F.);
#16743=ORIENTED_EDGE('',*,*,#12913,.F.);
#16744=ORIENTED_EDGE('',*,*,#12920,.T.);
#16745=ORIENTED_EDGE('',*,*,#12917,.T.);
#16746=ORIENTED_EDGE('',*,*,#12920,.F.);
#16747=ORIENTED_EDGE('',*,*,#12916,.F.);
#16748=ORIENTED_EDGE('',*,*,#12910,.T.);
#16749=ORIENTED_EDGE('',*,*,#12921,.T.);
#16750=ORIENTED_EDGE('',*,*,#12922,.T.);
#16751=ORIENTED_EDGE('',*,*,#12923,.F.);
#16752=ORIENTED_EDGE('',*,*,#12924,.T.);
#16753=ORIENTED_EDGE('',*,*,#12925,.F.);
#16754=ORIENTED_EDGE('',*,*,#12926,.T.);
#16755=ORIENTED_EDGE('',*,*,#12927,.T.);
#16756=ORIENTED_EDGE('',*,*,#12926,.F.);
#16757=ORIENTED_EDGE('',*,*,#12928,.T.);
#16758=ORIENTED_EDGE('',*,*,#12929,.T.);
#16759=ORIENTED_EDGE('',*,*,#12930,.F.);
#16760=ORIENTED_EDGE('',*,*,#12931,.T.);
#16761=ORIENTED_EDGE('',*,*,#12932,.T.);
#16762=ORIENTED_EDGE('',*,*,#12933,.T.);
#16763=ORIENTED_EDGE('',*,*,#12934,.F.);
#16764=ORIENTED_EDGE('',*,*,#12935,.T.);
#16765=ORIENTED_EDGE('',*,*,#12936,.T.);
#16766=ORIENTED_EDGE('',*,*,#12937,.T.);
#16767=ORIENTED_EDGE('',*,*,#12938,.F.);
#16768=ORIENTED_EDGE('',*,*,#12939,.T.);
#16769=ORIENTED_EDGE('',*,*,#12912,.T.);
#16770=ORIENTED_EDGE('',*,*,#12925,.T.);
#16771=ORIENTED_EDGE('',*,*,#12919,.F.);
#16772=ORIENTED_EDGE('',*,*,#12930,.T.);
#16773=ORIENTED_EDGE('',*,*,#12940,.T.);
#16774=ORIENTED_EDGE('',*,*,#12923,.T.);
#16775=ORIENTED_EDGE('',*,*,#12941,.T.);
#16776=ORIENTED_EDGE('',*,*,#12938,.T.);
#16777=ORIENTED_EDGE('',*,*,#12942,.T.);
#16778=ORIENTED_EDGE('',*,*,#12934,.T.);
#16779=ORIENTED_EDGE('',*,*,#12943,.T.);
#16780=ORIENTED_EDGE('',*,*,#12927,.F.);
#16781=ORIENTED_EDGE('',*,*,#12921,.F.);
#16782=ORIENTED_EDGE('',*,*,#12944,.T.);
#16783=ORIENTED_EDGE('',*,*,#12928,.F.);
#16784=ORIENTED_EDGE('',*,*,#12945,.T.);
#16785=ORIENTED_EDGE('',*,*,#12932,.F.);
#16786=ORIENTED_EDGE('',*,*,#12946,.T.);
#16787=ORIENTED_EDGE('',*,*,#12936,.F.);
#16788=ORIENTED_EDGE('',*,*,#12947,.T.);
#16789=ORIENTED_EDGE('',*,*,#12915,.T.);
#16790=ORIENTED_EDGE('',*,*,#12947,.F.);
#16791=ORIENTED_EDGE('',*,*,#12939,.F.);
#16792=ORIENTED_EDGE('',*,*,#12941,.F.);
#16793=ORIENTED_EDGE('',*,*,#12922,.F.);
#16794=ORIENTED_EDGE('',*,*,#12946,.F.);
#16795=ORIENTED_EDGE('',*,*,#12935,.F.);
#16796=ORIENTED_EDGE('',*,*,#12942,.F.);
#16797=ORIENTED_EDGE('',*,*,#12937,.F.);
#16798=ORIENTED_EDGE('',*,*,#12945,.F.);
#16799=ORIENTED_EDGE('',*,*,#12931,.F.);
#16800=ORIENTED_EDGE('',*,*,#12943,.F.);
#16801=ORIENTED_EDGE('',*,*,#12933,.F.);
#16802=ORIENTED_EDGE('',*,*,#12944,.F.);
#16803=ORIENTED_EDGE('',*,*,#12924,.F.);
#16804=ORIENTED_EDGE('',*,*,#12940,.F.);
#16805=ORIENTED_EDGE('',*,*,#12929,.F.);
#16806=ORIENTED_EDGE('',*,*,#12948,.F.);
#16807=ORIENTED_EDGE('',*,*,#12949,.T.);
#16808=ORIENTED_EDGE('',*,*,#12950,.F.);
#16809=ORIENTED_EDGE('',*,*,#12949,.F.);
#16810=ORIENTED_EDGE('',*,*,#12951,.T.);
#16811=ORIENTED_EDGE('',*,*,#12952,.T.);
#16812=ORIENTED_EDGE('',*,*,#12953,.F.);
#16813=ORIENTED_EDGE('',*,*,#12952,.F.);
#16814=ORIENTED_EDGE('',*,*,#12954,.T.);
#16815=ORIENTED_EDGE('',*,*,#12951,.F.);
#16816=ORIENTED_EDGE('',*,*,#12955,.T.);
#16817=ORIENTED_EDGE('',*,*,#12948,.T.);
#16818=ORIENTED_EDGE('',*,*,#12955,.F.);
#16819=ORIENTED_EDGE('',*,*,#12954,.F.);
#16820=ORIENTED_EDGE('',*,*,#12953,.T.);
#16821=ORIENTED_EDGE('',*,*,#12950,.T.);
#16822=ORIENTED_EDGE('',*,*,#12956,.F.);
#16823=ORIENTED_EDGE('',*,*,#12957,.F.);
#16824=ORIENTED_EDGE('',*,*,#12958,.F.);
#16825=ORIENTED_EDGE('',*,*,#12959,.F.);
#16826=ORIENTED_EDGE('',*,*,#12960,.F.);
#16827=ORIENTED_EDGE('',*,*,#12961,.F.);
#16828=ORIENTED_EDGE('',*,*,#12956,.T.);
#16829=ORIENTED_EDGE('',*,*,#12962,.F.);
#16830=ORIENTED_EDGE('',*,*,#12963,.F.);
#16831=ORIENTED_EDGE('',*,*,#12964,.T.);
#16832=ORIENTED_EDGE('',*,*,#12957,.T.);
#16833=ORIENTED_EDGE('',*,*,#12964,.F.);
#16834=ORIENTED_EDGE('',*,*,#12965,.F.);
#16835=ORIENTED_EDGE('',*,*,#12966,.T.);
#16836=ORIENTED_EDGE('',*,*,#12958,.T.);
#16837=ORIENTED_EDGE('',*,*,#12966,.F.);
#16838=ORIENTED_EDGE('',*,*,#12967,.F.);
#16839=ORIENTED_EDGE('',*,*,#12968,.T.);
#16840=ORIENTED_EDGE('',*,*,#12959,.T.);
#16841=ORIENTED_EDGE('',*,*,#12968,.F.);
#16842=ORIENTED_EDGE('',*,*,#12969,.F.);
#16843=ORIENTED_EDGE('',*,*,#12970,.T.);
#16844=ORIENTED_EDGE('',*,*,#12960,.T.);
#16845=ORIENTED_EDGE('',*,*,#12970,.F.);
#16846=ORIENTED_EDGE('',*,*,#12971,.F.);
#16847=ORIENTED_EDGE('',*,*,#12972,.T.);
#16848=ORIENTED_EDGE('',*,*,#12961,.T.);
#16849=ORIENTED_EDGE('',*,*,#12972,.F.);
#16850=ORIENTED_EDGE('',*,*,#12973,.F.);
#16851=ORIENTED_EDGE('',*,*,#12962,.T.);
#16852=ORIENTED_EDGE('',*,*,#12963,.T.);
#16853=ORIENTED_EDGE('',*,*,#12973,.T.);
#16854=ORIENTED_EDGE('',*,*,#12971,.T.);
#16855=ORIENTED_EDGE('',*,*,#12969,.T.);
#16856=ORIENTED_EDGE('',*,*,#12967,.T.);
#16857=ORIENTED_EDGE('',*,*,#12965,.T.);
#22791=CYLINDRICAL_SURFACE('',#25215,1.621);
#22792=CYLINDRICAL_SURFACE('',#25223,5.4585);
#22793=CYLINDRICAL_SURFACE('',#25224,11.);
#22794=CYLINDRICAL_SURFACE('',#25227,8.5);
#22795=CYLINDRICAL_SURFACE('',#25230,11.);
#22796=CYLINDRICAL_SURFACE('',#25233,11.);
#22797=CYLINDRICAL_SURFACE('',#25236,11.);
#22798=CYLINDRICAL_SURFACE('',#25253,2.);
#23333=ADVANCED_FACE('',(#2341),#22791,.F.);
#23334=ADVANCED_FACE('',(#2342),#2118,.F.);
#23335=ADVANCED_FACE('',(#2343),#2119,.F.);
#23336=ADVANCED_FACE('',(#2344,#1069),#22792,.F.);
#23337=ADVANCED_FACE('',(#2345),#22793,.T.);
#23338=ADVANCED_FACE('',(#2346),#22794,.T.);
#23339=ADVANCED_FACE('',(#2347),#22795,.T.);
#23340=ADVANCED_FACE('',(#2348),#22796,.T.);
#23341=ADVANCED_FACE('',(#2349,#1070),#22797,.T.);
#23342=ADVANCED_FACE('',(#2350,#1071),#1454,.F.);
#23343=ADVANCED_FACE('',(#2351,#1072),#1455,.F.);
#23344=ADVANCED_FACE('',(#2352,#1073),#1456,.F.);
#23345=ADVANCED_FACE('',(#2353),#1457,.F.);
#23346=ADVANCED_FACE('',(#2354),#1458,.F.);
#23347=ADVANCED_FACE('',(#2355),#1459,.F.);
#23348=ADVANCED_FACE('',(#2356),#1460,.F.);
#23349=ADVANCED_FACE('',(#2357),#2120,.T.);
#23350=ADVANCED_FACE('',(#2358),#2121,.T.);
#23351=ADVANCED_FACE('',(#2359),#22798,.T.);
#23352=ADVANCED_FACE('',(#2360),#1461,.T.);
#23353=ADVANCED_FACE('',(#2361,#1074),#1462,.T.);
#23354=ADVANCED_FACE('',(#2362),#1463,.F.);
#23355=ADVANCED_FACE('',(#2363),#1464,.F.);
#23356=ADVANCED_FACE('',(#2364),#1465,.F.);
#23357=ADVANCED_FACE('',(#2365),#1466,.F.);
#23358=ADVANCED_FACE('',(#2366),#1467,.F.);
#23359=ADVANCED_FACE('',(#2367),#1468,.F.);
#23360=ADVANCED_FACE('',(#2368),#1469,.T.);
#24530=CLOSED_SHELL('',(#23333,#23334,#23335,#23336,#23337,#23338,#23339,
#23340,#23341,#23342,#23343,#23344,#23345,#23346,#23347,#23348));
#24531=CLOSED_SHELL('',(#23349,#23350,#23351,#23352,#23353,#23354,#23355,
#23356,#23357,#23358,#23359,#23360));
#25214=AXIS2_PLACEMENT_3D('',#35656,#28394,#28395);
#25215=AXIS2_PLACEMENT_3D('',#35657,#28396,#28397);
#25216=AXIS2_PLACEMENT_3D('',#35729,#28399,#28400);
#25217=AXIS2_PLACEMENT_3D('',#35732,#28401,#28402);
#25218=AXIS2_PLACEMENT_3D('',#35735,#28404,#28405);
#25219=AXIS2_PLACEMENT_3D('',#35736,#28406,#28407);
#25220=AXIS2_PLACEMENT_3D('',#35737,#28408,#28409);
#25221=AXIS2_PLACEMENT_3D('',#35739,#28410,#28411);
#25222=AXIS2_PLACEMENT_3D('',#35742,#28413,#28414);
#25223=AXIS2_PLACEMENT_3D('',#35743,#28415,#28416);
#25224=AXIS2_PLACEMENT_3D('',#35745,#28418,#28419);
#25225=AXIS2_PLACEMENT_3D('',#35748,#28420,#28421);
#25226=AXIS2_PLACEMENT_3D('',#35752,#28423,#28424);
#25227=AXIS2_PLACEMENT_3D('',#35754,#28426,#28427);
#25228=AXIS2_PLACEMENT_3D('',#35756,#28428,#28429);
#25229=AXIS2_PLACEMENT_3D('',#35759,#28431,#28432);
#25230=AXIS2_PLACEMENT_3D('',#35760,#28433,#28434);
#25231=AXIS2_PLACEMENT_3D('',#35763,#28435,#28436);
#25232=AXIS2_PLACEMENT_3D('',#35767,#28438,#28439);
#25233=AXIS2_PLACEMENT_3D('',#35769,#28441,#28442);
#25234=AXIS2_PLACEMENT_3D('',#35772,#28443,#28444);
#25235=AXIS2_PLACEMENT_3D('',#35776,#28446,#28447);
#25236=AXIS2_PLACEMENT_3D('',#35778,#28449,#28450);
#25237=AXIS2_PLACEMENT_3D('',#35781,#28451,#28452);
#25238=AXIS2_PLACEMENT_3D('',#35785,#28454,#28455);
#25239=AXIS2_PLACEMENT_3D('',#35787,#28457,#28458);
#25240=AXIS2_PLACEMENT_3D('',#35788,#28459,#28460);
#25241=AXIS2_PLACEMENT_3D('',#35793,#28465,#28466);
#25242=AXIS2_PLACEMENT_3D('',#35798,#28471,#28472);
#25243=AXIS2_PLACEMENT_3D('',#35799,#28473,#28474);
#25244=AXIS2_PLACEMENT_3D('',#35800,#28475,#28476);
#25245=AXIS2_PLACEMENT_3D('',#35801,#28477,#28478);
#25246=AXIS2_PLACEMENT_3D('',#35802,#28479,#28480);
#25247=AXIS2_PLACEMENT_3D('',#35804,#28481,#28482);
#25248=AXIS2_PLACEMENT_3D('',#35807,#28484,#28485);
#25249=AXIS2_PLACEMENT_3D('',#35808,#28486,#28487);
#25250=AXIS2_PLACEMENT_3D('',#35811,#28488,#28489);
#25251=AXIS2_PLACEMENT_3D('',#35814,#28491,#28492);
#25252=AXIS2_PLACEMENT_3D('',#35815,#28493,#28494);
#25253=AXIS2_PLACEMENT_3D('',#35816,#28495,#28496);
#25254=AXIS2_PLACEMENT_3D('',#35818,#28498,#28499);
#25255=AXIS2_PLACEMENT_3D('',#35819,#28500,#28501);
#25256=AXIS2_PLACEMENT_3D('',#35832,#28508,#28509);
#25257=AXIS2_PLACEMENT_3D('',#35838,#28513,#28514);
#25258=AXIS2_PLACEMENT_3D('',#35842,#28517,#28518);
#25259=AXIS2_PLACEMENT_3D('',#35846,#28521,#28522);
#25260=AXIS2_PLACEMENT_3D('',#35850,#28525,#28526);
#25261=AXIS2_PLACEMENT_3D('',#35854,#28529,#28530);
#25262=AXIS2_PLACEMENT_3D('',#35856,#28532,#28533);
#28394=DIRECTION('axis',(0.,0.,1.));
#28395=DIRECTION('refdir',(1.,0.,0.));
#28396=DIRECTION('center_axis',(0.,1.,0.));
#28397=DIRECTION('ref_axis',(0.,0.,1.));
#28398=DIRECTION('',(0.,1.,0.));
#28399=DIRECTION('center_axis',(1.,0.,0.));
#28400=DIRECTION('ref_axis',(0.,0.,-1.));
#28401=DIRECTION('center_axis',(-1.,0.,0.));
#28402=DIRECTION('ref_axis',(0.,0.,1.));
#28403=DIRECTION('',(0.707106781186548,-8.65956056235493E-17,0.707106781186547));
#28404=DIRECTION('center_axis',(-1.,0.,0.));
#28405=DIRECTION('ref_axis',(0.,0.,1.));
#28406=DIRECTION('center_axis',(-1.,0.,0.));
#28407=DIRECTION('ref_axis',(0.,0.,1.));
#28408=DIRECTION('center_axis',(-1.,0.,0.));
#28409=DIRECTION('ref_axis',(0.,0.,1.));
#28410=DIRECTION('center_axis',(-1.,0.,0.));
#28411=DIRECTION('ref_axis',(0.,0.,1.));
#28412=DIRECTION('',(-0.707106781186547,-8.65956056235494E-17,-0.707106781186548));
#28413=DIRECTION('center_axis',(-1.,0.,0.));
#28414=DIRECTION('ref_axis',(0.,0.,1.));
#28415=DIRECTION('center_axis',(-1.,0.,0.));
#28416=DIRECTION('ref_axis',(0.,0.,1.));
#28417=DIRECTION('',(-1.,0.,0.));
#28418=DIRECTION('center_axis',(-1.,0.,0.));
#28419=DIRECTION('ref_axis',(0.,0.,1.));
#28420=DIRECTION('center_axis',(-1.,0.,0.));
#28421=DIRECTION('ref_axis',(0.,0.,1.));
#28422=DIRECTION('',(-1.,0.,0.));
#28423=DIRECTION('center_axis',(-1.,0.,0.));
#28424=DIRECTION('ref_axis',(0.,0.,1.));
#28425=DIRECTION('',(1.,0.,0.));
#28426=DIRECTION('center_axis',(-1.,0.,0.));
#28427=DIRECTION('ref_axis',(0.,0.,1.));
#28428=DIRECTION('center_axis',(-1.,0.,0.));
#28429=DIRECTION('ref_axis',(0.,0.,1.));
#28430=DIRECTION('',(1.,0.,0.));
#28431=DIRECTION('center_axis',(-1.,0.,0.));
#28432=DIRECTION('ref_axis',(0.,0.,1.));
#28433=DIRECTION('center_axis',(-1.,0.,0.));
#28434=DIRECTION('ref_axis',(0.,0.,1.));
#28435=DIRECTION('center_axis',(-1.,0.,0.));
#28436=DIRECTION('ref_axis',(0.,0.,1.));
#28437=DIRECTION('',(-1.,0.,0.));
#28438=DIRECTION('center_axis',(-1.,0.,0.));
#28439=DIRECTION('ref_axis',(0.,0.,1.));
#28440=DIRECTION('',(1.,0.,0.));
#28441=DIRECTION('center_axis',(-1.,0.,0.));
#28442=DIRECTION('ref_axis',(0.,1.22464679914735E-16,-1.));
#28443=DIRECTION('center_axis',(-1.,0.,0.));
#28444=DIRECTION('ref_axis',(0.,0.,1.));
#28445=DIRECTION('',(-1.,0.,0.));
#28446=DIRECTION('center_axis',(-1.,0.,0.));
#28447=DIRECTION('ref_axis',(0.,0.,1.));
#28448=DIRECTION('',(1.,0.,0.));
#28449=DIRECTION('center_axis',(-1.,0.,0.));
#28450=DIRECTION('ref_axis',(0.,0.,1.));
#28451=DIRECTION('center_axis',(-1.,0.,0.));
#28452=DIRECTION('ref_axis',(0.,0.,1.));
#28453=DIRECTION('',(-1.,0.,0.));
#28454=DIRECTION('center_axis',(-1.,0.,0.));
#28455=DIRECTION('ref_axis',(0.,0.,1.));
#28456=DIRECTION('',(1.,0.,0.));
#28457=DIRECTION('center_axis',(1.,0.,0.));
#28458=DIRECTION('ref_axis',(0.,0.,-1.));
#28459=DIRECTION('center_axis',(1.,0.,0.));
#28460=DIRECTION('ref_axis',(0.,0.,-1.));
#28461=DIRECTION('',(0.,0.707106781186548,0.707106781186548));
#28462=DIRECTION('',(0.,0.707106781186547,-0.707106781186547));
#28463=DIRECTION('',(0.,-0.707106781186547,-0.707106781186547));
#28464=DIRECTION('',(0.,-0.707106781186548,0.707106781186548));
#28465=DIRECTION('center_axis',(-1.,0.,0.));
#28466=DIRECTION('ref_axis',(0.,0.,1.));
#28467=DIRECTION('',(0.,-0.707106781186548,-0.707106781186548));
#28468=DIRECTION('',(0.,0.707106781186548,-0.707106781186548));
#28469=DIRECTION('',(0.,0.707106781186547,0.707106781186547));
#28470=DIRECTION('',(0.,-0.707106781186547,0.707106781186547));
#28471=DIRECTION('center_axis',(0.,-0.707106781186548,-0.707106781186548));
#28472=DIRECTION('ref_axis',(0.,0.707106781186548,-0.707106781186548));
#28473=DIRECTION('center_axis',(0.,-0.707106781186548,0.707106781186548));
#28474=DIRECTION('ref_axis',(0.,-0.707106781186548,-0.707106781186548));
#28475=DIRECTION('center_axis',(0.,0.707106781186547,0.707106781186548));
#28476=DIRECTION('ref_axis',(0.,-0.707106781186548,0.707106781186547));
#28477=DIRECTION('center_axis',(0.,0.707106781186548,-0.707106781186547));
#28478=DIRECTION('ref_axis',(0.,0.707106781186547,0.707106781186548));
#28479=DIRECTION('center_axis',(0.,-1.,0.));
#28480=DIRECTION('ref_axis',(0.,0.,-1.));
#28481=DIRECTION('center_axis',(0.,-1.,0.));
#28482=DIRECTION('ref_axis',(0.,0.,1.));
#28483=DIRECTION('',(8.65956056235491E-17,0.70710678118655,-0.707106781186545));
#28484=DIRECTION('center_axis',(0.,1.,0.));
#28485=DIRECTION('ref_axis',(0.,0.,1.));
#28486=DIRECTION('center_axis',(0.,1.,0.));
#28487=DIRECTION('ref_axis',(0.,0.,1.));
#28488=DIRECTION('center_axis',(0.,-1.,0.));
#28489=DIRECTION('ref_axis',(0.,0.,-1.));
#28490=DIRECTION('',(8.65956056235495E-17,-0.707106781186546,0.707106781186549));
#28491=DIRECTION('center_axis',(0.,-1.,0.));
#28492=DIRECTION('ref_axis',(0.,0.,-1.));
#28493=DIRECTION('center_axis',(0.,-1.,0.));
#28494=DIRECTION('ref_axis',(0.,0.,-1.));
#28495=DIRECTION('center_axis',(0.,-1.,0.));
#28496=DIRECTION('ref_axis',(0.,0.,-1.));
#28497=DIRECTION('',(0.,1.,0.));
#28498=DIRECTION('center_axis',(0.,-1.,0.));
#28499=DIRECTION('ref_axis',(0.,0.,-1.));
#28500=DIRECTION('center_axis',(0.,1.,0.));
#28501=DIRECTION('ref_axis',(0.,0.,1.));
#28502=DIRECTION('',(-0.866025403784439,0.,-0.5));
#28503=DIRECTION('',(0.,0.,-1.));
#28504=DIRECTION('',(0.866025403784439,0.,-0.5));
#28505=DIRECTION('',(0.866025403784439,0.,0.5));
#28506=DIRECTION('',(7.5115729936858E-16,0.,1.));
#28507=DIRECTION('',(-0.866025403784439,0.,0.5));
#28508=DIRECTION('center_axis',(0.5,0.,-0.866025403784439));
#28509=DIRECTION('ref_axis',(-0.866025403784439,0.,-0.5));
#28510=DIRECTION('',(0.,1.,0.));
#28511=DIRECTION('',(-0.866025403784439,0.,-0.5));
#28512=DIRECTION('',(0.,1.,0.));
#28513=DIRECTION('center_axis',(1.,0.,0.));
#28514=DIRECTION('ref_axis',(0.,0.,-1.));
#28515=DIRECTION('',(0.,0.,-1.));
#28516=DIRECTION('',(0.,1.,0.));
#28517=DIRECTION('center_axis',(0.5,0.,0.866025403784439));
#28518=DIRECTION('ref_axis',(0.866025403784439,0.,-0.5));
#28519=DIRECTION('',(0.866025403784439,0.,-0.5));
#28520=DIRECTION('',(0.,1.,0.));
#28521=DIRECTION('center_axis',(-0.5,0.,0.866025403784439));
#28522=DIRECTION('ref_axis',(0.866025403784439,0.,0.5));
#28523=DIRECTION('',(0.866025403784439,0.,0.5));
#28524=DIRECTION('',(0.,1.,0.));
#28525=DIRECTION('center_axis',(-1.,0.,7.5115729936858E-16));
#28526=DIRECTION('ref_axis',(7.5115729936858E-16,0.,1.));
#28527=DIRECTION('',(7.5115729936858E-16,0.,1.));
#28528=DIRECTION('',(0.,1.,0.));
#28529=DIRECTION('center_axis',(-0.5,0.,-0.866025403784439));
#28530=DIRECTION('ref_axis',(-0.866025403784439,0.,0.5));
#28531=DIRECTION('',(-0.866025403784439,0.,0.5));
#28532=DIRECTION('center_axis',(0.,1.,0.));
#28533=DIRECTION('ref_axis',(0.,0.,1.));
#35656=CARTESIAN_POINT('',(0.,0.,0.));
#35657=CARTESIAN_POINT('Origin',(5.5,11.,0.));
#35658=CARTESIAN_POINT('',(5.5,5.21225299174935,-1.621));
#35659=CARTESIAN_POINT('Ctrl Pts',(5.5,5.21225299174935,-1.621));
#35660=CARTESIAN_POINT('Ctrl Pts',(5.29509392838307,5.21225299174935,-1.621));
#35661=CARTESIAN_POINT('Ctrl Pts',(5.07744240259474,5.22560045988912,-1.57979528744991));
#35662=CARTESIAN_POINT('Ctrl Pts',(4.67846794933173,5.27287962307746,-1.41399911891084));
#35663=CARTESIAN_POINT('Ctrl Pts',(4.49702782444847,5.30603062902532,-1.28946800905525));
#35664=CARTESIAN_POINT('Ctrl Pts',(4.21057289219421,5.36755449841623,-1.00301307680099));
#35665=CARTESIAN_POINT('Ctrl Pts',(4.08601009499387,5.4000554117724,-0.821556304277599));
#35666=CARTESIAN_POINT('Ctrl Pts',(3.92019054985229,5.44582673671694,-0.422521434885201));
#35667=CARTESIAN_POINT('Ctrl Pts',(3.879,5.4585,-0.204847565255781));
#35668=CARTESIAN_POINT('Ctrl Pts',(3.879,5.4585,0.204847565255781));
#35669=CARTESIAN_POINT('Ctrl Pts',(3.92019054985229,5.44582673671694,0.422521434885201));
#35670=CARTESIAN_POINT('Ctrl Pts',(4.08601009499387,5.4000554117724,0.821556304277599));
#35671=CARTESIAN_POINT('Ctrl Pts',(4.21057289219421,5.36755449841623,1.00301307680099));
#35672=CARTESIAN_POINT('Ctrl Pts',(4.49702782444847,5.30603062902532,1.28946800905525));
#35673=CARTESIAN_POINT('Ctrl Pts',(4.67846794933173,5.27287962307746,1.41399911891084));
#35674=CARTESIAN_POINT('Ctrl Pts',(5.07744240259474,5.22560045988912,1.57979528744991));
#35675=CARTESIAN_POINT('Ctrl Pts',(5.29509392838307,5.21225299174935,1.621));
#35676=CARTESIAN_POINT('Ctrl Pts',(5.70490607161693,5.21225299174935,1.621));
#35677=CARTESIAN_POINT('Ctrl Pts',(5.92255759740526,5.22560045988912,1.57979528744991));
#35678=CARTESIAN_POINT('Ctrl Pts',(6.32153205066828,5.27287962307746,1.41399911891084));
#35679=CARTESIAN_POINT('Ctrl Pts',(6.50297217555153,5.30603062902532,1.28946800905525));
#35680=CARTESIAN_POINT('Ctrl Pts',(6.78942710780579,5.36755449841623,1.00301307680099));
#35681=CARTESIAN_POINT('Ctrl Pts',(6.91398990500613,5.4000554117724,0.8215563042776));
#35682=CARTESIAN_POINT('Ctrl Pts',(7.07980945014771,5.44582673671694,0.422521434885203));
#35683=CARTESIAN_POINT('Ctrl Pts',(7.121,5.4585,0.204847565255782));
#35684=CARTESIAN_POINT('Ctrl Pts',(7.121,5.4585,-0.20484756525578));
#35685=CARTESIAN_POINT('Ctrl Pts',(7.07980945014771,5.44582673671694,-0.422521434885202));
#35686=CARTESIAN_POINT('Ctrl Pts',(6.91398990500613,5.4000554117724,-0.821556304277599));
#35687=CARTESIAN_POINT('Ctrl Pts',(6.78942710780579,5.36755449841623,-1.00301307680099));
#35688=CARTESIAN_POINT('Ctrl Pts',(6.50297217555153,5.30603062902532,-1.28946800905525));
#35689=CARTESIAN_POINT('Ctrl Pts',(6.32153205066828,5.27287962307746,-1.41399911891084));
#35690=CARTESIAN_POINT('Ctrl Pts',(5.92255759740526,5.22560045988912,-1.57979528744991));
#35691=CARTESIAN_POINT('Ctrl Pts',(5.70490607161694,5.21225299174935,-1.621));
#35692=CARTESIAN_POINT('Ctrl Pts',(5.5,5.21225299174935,-1.621));
#35693=CARTESIAN_POINT('',(5.5,10.8799062036398,-1.621));
#35694=CARTESIAN_POINT('',(5.5,11.,-1.621));
#35695=CARTESIAN_POINT('Ctrl Pts',(5.5,10.8799062036398,-1.621));
#35696=CARTESIAN_POINT('Ctrl Pts',(5.7038572300951,10.8799062036398,-1.621));
#35697=CARTESIAN_POINT('Ctrl Pts',(5.92109642242532,10.8862276408641,-1.58019820547013));
#35698=CARTESIAN_POINT('Ctrl Pts',(6.32038751501911,10.9089717931152,-1.41467769063433));
#35699=CARTESIAN_POINT('Ctrl Pts',(6.5024652295479,10.9250563808622,-1.28997495505889));
#35700=CARTESIAN_POINT('Ctrl Pts',(6.78997262190052,10.9551791595233,-1.00246756270627));
#35701=CARTESIAN_POINT('Ctrl Pts',(6.91467718754251,10.9711871972319,-0.82038884065458));
#35702=CARTESIAN_POINT('Ctrl Pts',(7.08019903497012,10.9937557707836,-0.421094309383512));
#35703=CARTESIAN_POINT('Ctrl Pts',(7.121,11.,-0.203853921468213));
#35704=CARTESIAN_POINT('Ctrl Pts',(7.121,11.,0.203853921468214));
#35705=CARTESIAN_POINT('Ctrl Pts',(7.08019903497012,10.9937557707836,0.421094309383513));
#35706=CARTESIAN_POINT('Ctrl Pts',(6.91467718754251,10.9711871972319,0.820388840654582));
#35707=CARTESIAN_POINT('Ctrl Pts',(6.78997262190052,10.9551791595233,1.00246756270627));
#35708=CARTESIAN_POINT('Ctrl Pts',(6.5024652295479,10.9250563808622,1.28997495505889));
#35709=CARTESIAN_POINT('Ctrl Pts',(6.32038751501911,10.9089717931152,1.41467769063433));
#35710=CARTESIAN_POINT('Ctrl Pts',(5.92109642242532,10.8862276408641,1.58019820547013));
#35711=CARTESIAN_POINT('Ctrl Pts',(5.7038572300951,10.8799062036398,1.621));
#35712=CARTESIAN_POINT('Ctrl Pts',(5.29614276990491,10.8799062036398,1.621));
#35713=CARTESIAN_POINT('Ctrl Pts',(5.07890357757468,10.8862276408641,1.58019820547013));
#35714=CARTESIAN_POINT('Ctrl Pts',(4.6796124849809,10.9089717931152,1.41467769063433));
#35715=CARTESIAN_POINT('Ctrl Pts',(4.49753477045211,10.9250563808622,1.28997495505889));
#35716=CARTESIAN_POINT('Ctrl Pts',(4.21002737809948,10.9551791595233,1.00246756270627));
#35717=CARTESIAN_POINT('Ctrl Pts',(4.08532281245749,10.9711871972319,0.820388840654582));
#35718=CARTESIAN_POINT('Ctrl Pts',(3.91980096502989,10.9937557707836,0.421094309383513));
#35719=CARTESIAN_POINT('Ctrl Pts',(3.879,11.,0.203853921468214));
#35720=CARTESIAN_POINT('Ctrl Pts',(3.879,11.,-0.203853921468214));
#35721=CARTESIAN_POINT('Ctrl Pts',(3.91980096502989,10.9937557707836,-0.421094309383514));
#35722=CARTESIAN_POINT('Ctrl Pts',(4.08532281245749,10.9711871972319,-0.820388840654582));
#35723=CARTESIAN_POINT('Ctrl Pts',(4.21002737809948,10.9551791595233,-1.00246756270627));
#35724=CARTESIAN_POINT('Ctrl Pts',(4.49753477045211,10.9250563808622,-1.28997495505889));
#35725=CARTESIAN_POINT('Ctrl Pts',(4.6796124849809,10.9089717931152,-1.41467769063433));
#35726=CARTESIAN_POINT('Ctrl Pts',(5.07890357757468,10.8862276408641,-1.58019820547013));
#35727=CARTESIAN_POINT('Ctrl Pts',(5.29614276990491,10.8799062036398,-1.621));
#35728=CARTESIAN_POINT('Ctrl Pts',(5.5,10.8799062036398,-1.621));
#35729=CARTESIAN_POINT('Origin',(7.4585,0.,0.));
#35730=CARTESIAN_POINT('',(7.4585,6.68473455314583E-16,-5.4585));
#35731=CARTESIAN_POINT('',(7.4585,-6.68473455314583E-16,5.4585));
#35732=CARTESIAN_POINT('Origin',(7.4585,0.,0.));
#35733=CARTESIAN_POINT('',(8.,-7.34788079488412E-16,6.));
#35734=CARTESIAN_POINT('',(7.4585,-6.68473455314583E-16,5.4585));
#35735=CARTESIAN_POINT('Origin',(8.,0.,0.));
#35736=CARTESIAN_POINT('Origin',(7.4585,0.,0.));
#35737=CARTESIAN_POINT('Origin',(0.,0.,0.));
#35738=CARTESIAN_POINT('',(0.541500000000001,-6.68473455314583E-16,-5.4585));
#35739=CARTESIAN_POINT('Origin',(0.5415,0.,0.));
#35740=CARTESIAN_POINT('',(-4.6168096649323E-16,-7.34788079488412E-16,-6.));
#35741=CARTESIAN_POINT('',(0.,-7.34788079488412E-16,-6.));
#35742=CARTESIAN_POINT('Origin',(0.,0.,0.));
#35743=CARTESIAN_POINT('Origin',(0.,0.,0.));
#35744=CARTESIAN_POINT('',(0.,-6.68473455314583E-16,-5.4585));
#35745=CARTESIAN_POINT('Origin',(-0.25,0.,0.));
#35746=CARTESIAN_POINT('',(8.,-2.79641763593266,10.6386112066117));
#35747=CARTESIAN_POINT('',(8.,2.79641763593267,10.6386112066117));
#35748=CARTESIAN_POINT('Origin',(8.,0.,0.));
#35749=CARTESIAN_POINT('',(1.,2.79641763593267,10.6386112066117));
#35750=CARTESIAN_POINT('',(-0.25,2.79641763593267,10.6386112066117));
#35751=CARTESIAN_POINT('',(1.,-2.79641763593267,10.6386112066117));
#35752=CARTESIAN_POINT('Origin',(1.,0.,0.));
#35753=CARTESIAN_POINT('',(-0.25,-2.79641763593267,10.6386112066117));
#35754=CARTESIAN_POINT('Origin',(-0.25,0.,0.));
#35755=CARTESIAN_POINT('',(0.,-1.04094977927525E-15,-8.5));
#35756=CARTESIAN_POINT('Origin',(0.,0.,0.));
#35757=CARTESIAN_POINT('',(1.,-1.04094977927525E-15,-8.5));
#35758=CARTESIAN_POINT('',(-0.25,-1.04094977927525E-15,-8.5));
#35759=CARTESIAN_POINT('Origin',(1.,0.,0.));
#35760=CARTESIAN_POINT('Origin',(-0.25,0.,0.));
#35761=CARTESIAN_POINT('',(8.,-10.6386112066117,-2.79641763593268));
#35762=CARTESIAN_POINT('',(8.,-10.6386112066117,2.79641763593267));
#35763=CARTESIAN_POINT('Origin',(8.,0.,0.));
#35764=CARTESIAN_POINT('',(1.,-10.6386112066117,2.79641763593267));
#35765=CARTESIAN_POINT('',(-0.25,-10.6386112066117,2.79641763593267));
#35766=CARTESIAN_POINT('',(1.,-10.6386112066117,-2.79641763593268));
#35767=CARTESIAN_POINT('Origin',(1.,0.,0.));
#35768=CARTESIAN_POINT('',(-0.25,-10.6386112066117,-2.79641763593268));
#35769=CARTESIAN_POINT('Origin',(-0.25,0.,0.));
#35770=CARTESIAN_POINT('',(8.,2.79641763593267,-10.6386112066117));
#35771=CARTESIAN_POINT('',(8.,-2.79641763593268,-10.6386112066117));
#35772=CARTESIAN_POINT('Origin',(8.,0.,0.));
#35773=CARTESIAN_POINT('',(1.,-2.79641763593268,-10.6386112066117));
#35774=CARTESIAN_POINT('',(-0.25,-2.79641763593268,-10.6386112066117));
#35775=CARTESIAN_POINT('',(1.,2.79641763593267,-10.6386112066117));
#35776=CARTESIAN_POINT('Origin',(1.,0.,0.));
#35777=CARTESIAN_POINT('',(-0.25,2.79641763593267,-10.6386112066117));
#35778=CARTESIAN_POINT('Origin',(-0.25,0.,0.));
#35779=CARTESIAN_POINT('',(8.,10.6386112066117,2.79641763593267));
#35780=CARTESIAN_POINT('',(8.,10.6386112066117,-2.79641763593267));
#35781=CARTESIAN_POINT('Origin',(8.,0.,0.));
#35782=CARTESIAN_POINT('',(1.,10.6386112066117,-2.79641763593267));
#35783=CARTESIAN_POINT('',(-0.25,10.6386112066117,-2.79641763593267));
#35784=CARTESIAN_POINT('',(1.,10.6386112066117,2.79641763593267));
#35785=CARTESIAN_POINT('Origin',(1.,0.,0.));
#35786=CARTESIAN_POINT('',(-0.25,10.6386112066117,2.79641763593267));
#35787=CARTESIAN_POINT('Origin',(0.,0.,0.));
#35788=CARTESIAN_POINT('Origin',(1.,8.5,0.));
#35789=CARTESIAN_POINT('',(1.,-2.4675144212722,10.9675144212722));
#35790=CARTESIAN_POINT('',(1.,10.9675144212722,2.4675144212722));
#35791=CARTESIAN_POINT('',(1.,10.9675144212722,-2.4675144212722));
#35792=CARTESIAN_POINT('',(1.,-2.4675144212722,-10.9675144212722));
#35793=CARTESIAN_POINT('Origin',(8.,11.,0.));
#35794=CARTESIAN_POINT('',(8.,-1.2175144212722,12.2175144212722));
#35795=CARTESIAN_POINT('',(8.,-1.2175144212722,-12.2175144212722));
#35796=CARTESIAN_POINT('',(8.,12.2175144212722,-1.2175144212722));
#35797=CARTESIAN_POINT('',(8.,12.2175144212722,1.2175144212722));
#35798=CARTESIAN_POINT('Origin',(8.,13.4350288425444,2.16840434497101E-16));
#35799=CARTESIAN_POINT('Origin',(8.,1.62630325872825E-16,-13.4350288425444));
#35800=CARTESIAN_POINT('Origin',(8.,1.62630325872825E-16,-13.4350288425444));
#35801=CARTESIAN_POINT('Origin',(8.,-13.4350288425444,-2.65629532258949E-15));
#35802=CARTESIAN_POINT('Origin',(5.5,10.8,0.));
#35803=CARTESIAN_POINT('',(5.5,10.8,2.));
#35804=CARTESIAN_POINT('Origin',(5.5,10.8,0.));
#35805=CARTESIAN_POINT('',(5.5,11.,1.8));
#35806=CARTESIAN_POINT('',(5.5,10.8,2.));
#35807=CARTESIAN_POINT('Origin',(5.5,11.,0.));
#35808=CARTESIAN_POINT('Origin',(5.5,6.,0.));
#35809=CARTESIAN_POINT('',(5.5,6.75,2.));
#35810=CARTESIAN_POINT('',(5.5,6.75,-2.));
#35811=CARTESIAN_POINT('Origin',(5.5,6.75,0.));
#35812=CARTESIAN_POINT('',(5.5,6.,-1.25));
#35813=CARTESIAN_POINT('',(5.5,6.,-1.25));
#35814=CARTESIAN_POINT('Origin',(5.5,6.,0.));
#35815=CARTESIAN_POINT('Origin',(5.5,6.75,0.));
#35816=CARTESIAN_POINT('Origin',(5.5,0.,0.));
#35817=CARTESIAN_POINT('',(5.5,0.,2.));
#35818=CARTESIAN_POINT('Origin',(5.5,6.,-1.25));
#35819=CARTESIAN_POINT('Origin',(5.5,11.,0.));
#35820=CARTESIAN_POINT('',(6.5,11.,-0.577350269189626));
#35821=CARTESIAN_POINT('',(5.5,11.,-1.15470053837925));
#35822=CARTESIAN_POINT('',(6.5,11.,-0.577350269189626));
#35823=CARTESIAN_POINT('',(6.5,11.,0.577350269189626));
#35824=CARTESIAN_POINT('',(6.5,11.,0.577350269189626));
#35825=CARTESIAN_POINT('',(5.5,11.,1.15470053837925));
#35826=CARTESIAN_POINT('',(5.5,11.,1.15470053837925));
#35827=CARTESIAN_POINT('',(4.5,11.,0.577350269189625));
#35828=CARTESIAN_POINT('',(4.5,11.,0.577350269189625));
#35829=CARTESIAN_POINT('',(4.5,11.,-0.577350269189626));
#35830=CARTESIAN_POINT('',(4.5,11.,-0.577350269189626));
#35831=CARTESIAN_POINT('',(5.5,11.,-1.15470053837925));
#35832=CARTESIAN_POINT('Origin',(6.5,9.,-0.577350269189626));
#35833=CARTESIAN_POINT('',(5.5,9.,-1.15470053837925));
#35834=CARTESIAN_POINT('',(5.5,9.,-1.15470053837925));
#35835=CARTESIAN_POINT('',(6.5,9.,-0.577350269189626));
#35836=CARTESIAN_POINT('',(6.5,9.,-0.577350269189626));
#35837=CARTESIAN_POINT('',(6.5,9.,-0.577350269189626));
#35838=CARTESIAN_POINT('Origin',(6.5,9.,0.577350269189626));
#35839=CARTESIAN_POINT('',(6.5,9.,0.577350269189626));
#35840=CARTESIAN_POINT('',(6.5,9.,0.577350269189626));
#35841=CARTESIAN_POINT('',(6.5,9.,0.577350269189626));
#35842=CARTESIAN_POINT('Origin',(5.5,9.,1.15470053837925));
#35843=CARTESIAN_POINT('',(5.5,9.,1.15470053837925));
#35844=CARTESIAN_POINT('',(5.5,9.,1.15470053837925));
#35845=CARTESIAN_POINT('',(5.5,9.,1.15470053837925));
#35846=CARTESIAN_POINT('Origin',(4.5,9.,0.577350269189625));
#35847=CARTESIAN_POINT('',(4.5,9.,0.577350269189625));
#35848=CARTESIAN_POINT('',(4.5,9.,0.577350269189625));
#35849=CARTESIAN_POINT('',(4.5,9.,0.577350269189625));
#35850=CARTESIAN_POINT('Origin',(4.5,9.,-0.577350269189626));
#35851=CARTESIAN_POINT('',(4.5,9.,-0.577350269189626));
#35852=CARTESIAN_POINT('',(4.5,9.,-0.577350269189626));
#35853=CARTESIAN_POINT('',(4.5,9.,-0.577350269189626));
#35854=CARTESIAN_POINT('Origin',(5.5,9.,-1.15470053837925));
#35855=CARTESIAN_POINT('',(5.5,9.,-1.15470053837925));
#35856=CARTESIAN_POINT('Origin',(0.,9.,0.));
#57010=UNCERTAINTY_MEASURE_WITH_UNIT(LENGTH_MEASURE(0.01),#57080,
'DISTANCE_ACCURACY_VALUE',
'Maximum model space distance between geometric entities at asserted c
onnectivities');
#57040=UNCERTAINTY_MEASURE_WITH_UNIT(LENGTH_MEASURE(0.01),#57080,
'DISTANCE_ACCURACY_VALUE',
'Maximum model space distance between geometric entities at asserted c
onnectivities');
#57049=(
GEOMETRIC_REPRESENTATION_CONTEXT(3)
GLOBAL_UNCERTAINTY_ASSIGNED_CONTEXT((#57010))
GLOBAL_UNIT_ASSIGNED_CONTEXT((#57080,#57082,#57083))
REPRESENTATION_CONTEXT('','3D')
);
#57079=(
GEOMETRIC_REPRESENTATION_CONTEXT(3)
GLOBAL_UNCERTAINTY_ASSIGNED_CONTEXT((#57040))
GLOBAL_UNIT_ASSIGNED_CONTEXT((#57080,#57082,#57083))
REPRESENTATION_CONTEXT('','3D')
);
#57080=(
LENGTH_UNIT()
NAMED_UNIT(*)
SI_UNIT(.MILLI.,.METRE.)
);
#57082=(
NAMED_UNIT(*)
PLANE_ANGLE_UNIT()
SI_UNIT($,.RADIAN.)
);
#57083=(
NAMED_UNIT(*)
SI_UNIT($,.STERADIAN.)
SOLID_ANGLE_UNIT()
);
#57092=SHAPE_DEFINITION_REPRESENTATION(#57132,#57257);
#57132=PRODUCT_DEFINITION_SHAPE('',$,#57296);
#57257=SHAPE_REPRESENTATION('',(#25214),#57049);
#57287=PRODUCT_DEFINITION_CONTEXT('part definition',#57403,'design');
#57296=PRODUCT_DEFINITION('Lock Nut','Lock Nut',#57334,#57287);
#57334=PRODUCT_DEFINITION_FORMATION('',$,#57413);
#57403=APPLICATION_CONTEXT(
'Core Data for Automotive Mechanical Design Process');
#57404=PRODUCT_CONTEXT('part definition',#57403,'mechanical');
#57413=PRODUCT('Lock Nut','Lock Nut',$,(#57404));
#57444=PRESENTATION_STYLE_ASSIGNMENT((#57446));
#57446=SURFACE_STYLE_USAGE(.BOTH.,#57448);
#57448=SURFACE_SIDE_STYLE('',(#57450));
#57450=SURFACE_STYLE_FILL_AREA(#57452);
#57452=FILL_AREA_STYLE('Opaque(202,209,238)',(#57454));
#57454=FILL_AREA_STYLE_COLOUR('Opaque(202,209,238)',#57456);
#57456=COLOUR_RGB('Opaque(202,209,238)',0.792156862745098,0.819607843137255,
0.933333333333333);
ENDSEC;
END-ISO-10303-21;
